ISO-10303-21;
HEADER;
/* Generated by software containing ST-Developer
 * from STEP Tools, Inc. (www.steptools.com) 
 */

FILE_DESCRIPTION(
/* description */ ('Chain-less indexing wheel (Geneva) drive'),
/* implementation_level */ '2;1');

FILE_NAME(
/* name */ 'Foot strip (1).step',
/* time_stamp */ '2026-10-28T03:25:22-07:00',
/* author */ (''),
/* organization */ (''),
/* preprocessor_version */ 'ST-DEVELOPER v20.2',
/* originating_system */ 'Autodesk Translation Framework v15.17.0.0',
/* authorisation */ '');

FILE_SCHEMA (('AUTOMOTIVE_DESIGN { 1 0 10303 214 3 1 1 }'));
ENDSEC;

DATA;
#10=MECHANICAL_DESIGN_GEOMETRIC_PRESENTATION_REPRESENTATION('',(#305),#10957);
#255=SHAPE_REPRESENTATION_RELATIONSHIP('SRR','None',#11068,#280);
#280=ADVANCED_BREP_SHAPE_REPRESENTATION('',(#338),#10931);
#305=STYLED_ITEM('',(#11273),#338);
#338=MANIFOLD_SOLID_BREP('Body1',#5701);
#484=PLANE('',#6039);
#485=PLANE('',#6040);
#486=PLANE('',#6041);
#487=PLANE('',#6042);
#488=PLANE('',#6043);
#489=PLANE('',#6044);
#668=FACE_OUTER_BOUND('',#1009,.T.);
#669=FACE_OUTER_BOUND('',#1010,.T.);
#670=FACE_OUTER_BOUND('',#1011,.T.);
#671=FACE_OUTER_BOUND('',#1012,.T.);
#672=FACE_OUTER_BOUND('',#1013,.T.);
#673=FACE_OUTER_BOUND('',#1014,.T.);
#1009=EDGE_LOOP('',(#3819,#3820,#3821,#3822));
#1010=EDGE_LOOP('',(#3823,#3824,#3825,#3826));
#1011=EDGE_LOOP('',(#3827,#3828,#3829,#3830));
#1012=EDGE_LOOP('',(#3831,#3832,#3833,#3834));
#1013=EDGE_LOOP('',(#3835,#3836,#3837,#3838));
#1014=EDGE_LOOP('',(#3839,#3840,#3841,#3842));
#1451=LINE('',#8685,#1825);
#1452=LINE('',#8687,#1826);
#1453=LINE('',#8689,#1827);
#1454=LINE('',#8690,#1828);
#1455=LINE('',#8693,#1829);
#1456=LINE('',#8695,#1830);
#1457=LINE('',#8696,#1831);
#1458=LINE('',#8699,#1832);
#1459=LINE('',#8701,#1833);
#1460=LINE('',#8702,#1834);
#1461=LINE('',#8704,#1835);
#1462=LINE('',#8705,#1836);
#1825=VECTOR('',#6837,1.);
#1826=VECTOR('',#6838,1.);
#1827=VECTOR('',#6839,1.);
#1828=VECTOR('',#6840,1.);
#1829=VECTOR('',#6843,1.);
#1830=VECTOR('',#6844,1.);
#1831=VECTOR('',#6845,1.);
#1832=VECTOR('',#6848,1.);
#1833=VECTOR('',#6849,1.);
#1834=VECTOR('',#6850,1.);
#1835=VECTOR('',#6853,1.);
#1836=VECTOR('',#6854,1.);
#2529=VERTEX_POINT('',#8683);
#2530=VERTEX_POINT('',#8684);
#2531=VERTEX_POINT('',#8686);
#2532=VERTEX_POINT('',#8688);
#2533=VERTEX_POINT('',#8692);
#2534=VERTEX_POINT('',#8694);
#2535=VERTEX_POINT('',#8698);
#2536=VERTEX_POINT('',#8700);
#3035=EDGE_CURVE('',#2529,#2530,#1451,.T.);
#3036=EDGE_CURVE('',#2530,#2531,#1452,.T.);
#3037=EDGE_CURVE('',#2532,#2531,#1453,.T.);
#3038=EDGE_CURVE('',#2529,#2532,#1454,.T.);
#3039=EDGE_CURVE('',#2533,#2529,#1455,.T.);
#3040=EDGE_CURVE('',#2534,#2532,#1456,.T.);
#3041=EDGE_CURVE('',#2533,#2534,#1457,.T.);
#3042=EDGE_CURVE('',#2535,#2533,#1458,.T.);
#3043=EDGE_CURVE('',#2536,#2534,#1459,.T.);
#3044=EDGE_CURVE('',#2535,#2536,#1460,.T.);
#3045=EDGE_CURVE('',#2530,#2535,#1461,.T.);
#3046=EDGE_CURVE('',#2531,#2536,#1462,.T.);
#3819=ORIENTED_EDGE('',*,*,#3035,.T.);
#3820=ORIENTED_EDGE('',*,*,#3036,.T.);
#3821=ORIENTED_EDGE('',*,*,#3037,.F.);
#3822=ORIENTED_EDGE('',*,*,#3038,.F.);
#3823=ORIENTED_EDGE('',*,*,#3039,.T.);
#3824=ORIENTED_EDGE('',*,*,#3038,.T.);
#3825=ORIENTED_EDGE('',*,*,#3040,.F.);
#3826=ORIENTED_EDGE('',*,*,#3041,.F.);
#3827=ORIENTED_EDGE('',*,*,#3042,.T.);
#3828=ORIENTED_EDGE('',*,*,#3041,.T.);
#3829=ORIENTED_EDGE('',*,*,#3043,.F.);
#3830=ORIENTED_EDGE('',*,*,#3044,.F.);
#3831=ORIENTED_EDGE('',*,*,#3045,.T.);
#3832=ORIENTED_EDGE('',*,*,#3044,.T.);
#3833=ORIENTED_EDGE('',*,*,#3046,.F.);
#3834=ORIENTED_EDGE('',*,*,#3036,.F.);
#3835=ORIENTED_EDGE('',*,*,#3046,.T.);
#3836=ORIENTED_EDGE('',*,*,#3043,.T.);
#3837=ORIENTED_EDGE('',*,*,#3040,.T.);
#3838=ORIENTED_EDGE('',*,*,#3037,.T.);
#3839=ORIENTED_EDGE('',*,*,#3045,.F.);
#3840=ORIENTED_EDGE('',*,*,#3035,.F.);
#3841=ORIENTED_EDGE('',*,*,#3039,.F.);
#3842=ORIENTED_EDGE('',*,*,#3042,.F.);
#5382=ADVANCED_FACE('',(#668),#484,.T.);
#5383=ADVANCED_FACE('',(#669),#485,.T.);
#5384=ADVANCED_FACE('',(#670),#486,.T.);
#5385=ADVANCED_FACE('',(#671),#487,.T.);
#5386=ADVANCED_FACE('',(#672),#488,.T.);
#5387=ADVANCED_FACE('',(#673),#489,.F.);
#5701=CLOSED_SHELL('',(#5382,#5383,#5384,#5385,#5386,#5387));
#6038=AXIS2_PLACEMENT_3D('',#8681,#6833,#6834);
#6039=AXIS2_PLACEMENT_3D('',#8682,#6835,#6836);
#6040=AXIS2_PLACEMENT_3D('',#8691,#6841,#6842);
#6041=AXIS2_PLACEMENT_3D('',#8697,#6846,#6847);
#6042=AXIS2_PLACEMENT_3D('',#8703,#6851,#6852);
#6043=AXIS2_PLACEMENT_3D('',#8706,#6855,#6856);
#6044=AXIS2_PLACEMENT_3D('',#8707,#6857,#6858);
#6833=DIRECTION('axis',(0.,0.,1.));
#6834=DIRECTION('refdir',(1.,0.,0.));
#6835=DIRECTION('center_axis',(0.,1.,0.));
#6836=DIRECTION('ref_axis',(-1.,0.,0.));
#6837=DIRECTION('',(-1.,0.,0.));
#6838=DIRECTION('',(0.,0.,1.));
#6839=DIRECTION('',(-1.,0.,0.));
#6840=DIRECTION('',(0.,0.,1.));
#6841=DIRECTION('center_axis',(1.,0.,0.));
#6842=DIRECTION('ref_axis',(0.,1.,0.));
#6843=DIRECTION('',(0.,1.,0.));
#6844=DIRECTION('',(0.,1.,0.));
#6845=DIRECTION('',(0.,0.,1.));
#6846=DIRECTION('center_axis',(0.,-1.,0.));
#6847=DIRECTION('ref_axis',(1.,0.,0.));
#6848=DIRECTION('',(1.,0.,0.));
#6849=DIRECTION('',(1.,0.,0.));
#6850=DIRECTION('',(0.,0.,1.));
#6851=DIRECTION('center_axis',(-1.,0.,0.));
#6852=DIRECTION('ref_axis',(0.,-1.,0.));
#6853=DIRECTION('',(0.,-1.,0.));
#6854=DIRECTION('',(0.,-1.,0.));
#6855=DIRECTION('center_axis',(0.,0.,1.));
#6856=DIRECTION('ref_axis',(1.,0.,0.));
#6857=DIRECTION('center_axis',(0.,0.,1.));
#6858=DIRECTION('ref_axis',(1.,0.,0.));
#8681=CARTESIAN_POINT('',(0.,0.,0.));
#8682=CARTESIAN_POINT('Origin',(8.,4.,-0.6));
#8683=CARTESIAN_POINT('',(8.,4.,-0.6));
#8684=CARTESIAN_POINT('',(-3.5,4.,-0.6));
#8685=CARTESIAN_POINT('',(8.,4.,-0.6));
#8686=CARTESIAN_POINT('',(-3.5,4.,0.));
#8687=CARTESIAN_POINT('',(-3.5,4.,-0.6));
#8688=CARTESIAN_POINT('',(8.,4.,0.));
#8689=CARTESIAN_POINT('',(8.,4.,0.));
#8690=CARTESIAN_POINT('',(8.,4.,-0.6));
#8691=CARTESIAN_POINT('Origin',(8.,3.2,-0.6));
#8692=CARTESIAN_POINT('',(8.,3.2,-0.6));
#8693=CARTESIAN_POINT('',(8.,3.2,-0.6));
#8694=CARTESIAN_POINT('',(8.,3.2,0.));
#8695=CARTESIAN_POINT('',(8.,3.2,0.));
#8696=CARTESIAN_POINT('',(8.,3.2,-0.6));
#8697=CARTESIAN_POINT('Origin',(-3.5,3.2,-0.6));
#8698=CARTESIAN_POINT('',(-3.5,3.2,-0.6));
#8699=CARTESIAN_POINT('',(-3.5,3.2,-0.6));
#8700=CARTESIAN_POINT('',(-3.5,3.2,0.));
#8701=CARTESIAN_POINT('',(-3.5,3.2,0.));
#8702=CARTESIAN_POINT('',(-3.5,3.2,-0.6));
#8703=CARTESIAN_POINT('Origin',(-3.5,4.,-0.6));
#8704=CARTESIAN_POINT('',(-3.5,4.,-0.6));
#8705=CARTESIAN_POINT('',(-3.5,4.,0.));
#8706=CARTESIAN_POINT('Origin',(2.25,3.6,0.));
#8707=CARTESIAN_POINT('Origin',(2.25,3.6,-0.6));
#10900=UNCERTAINTY_MEASURE_WITH_UNIT(LENGTH_MEASURE(0.001),#10958,
'DISTANCE_ACCURACY_VALUE',
'Maximum model space distance between geometric entities at asserted c
onnectivities');
#10926=UNCERTAINTY_MEASURE_WITH_UNIT(LENGTH_MEASURE(0.001),#10958,
'DISTANCE_ACCURACY_VALUE',
'Maximum model space distance between geometric entities at asserted c
onnectivities');
#10931=(
GEOMETRIC_REPRESENTATION_CONTEXT(3)
GLOBAL_UNCERTAINTY_ASSIGNED_CONTEXT((#10900))
GLOBAL_UNIT_ASSIGNED_CONTEXT((#10958,#10960,#10961))
REPRESENTATION_CONTEXT('','3D')
);
#10957=(
GEOMETRIC_REPRESENTATION_CONTEXT(3)
GLOBAL_UNCERTAINTY_ASSIGNED_CONTEXT((#10926))
GLOBAL_UNIT_ASSIGNED_CONTEXT((#10958,#10960,#10961))
REPRESENTATION_CONTEXT('','3D')
);
#10958=(
LENGTH_UNIT()
NAMED_UNIT(*)
SI_UNIT(.CENTI.,.METRE.)
);
#10960=(
NAMED_UNIT(*)
PLANE_ANGLE_UNIT()
SI_UNIT($,.RADIAN.)
);
#10961=(
NAMED_UNIT(*)
SI_UNIT($,.STERADIAN.)
SOLID_ANGLE_UNIT()
);
#10966=SHAPE_DEFINITION_REPRESENTATION(#10996,#11068);
#10996=PRODUCT_DEFINITION_SHAPE('',$,#11099);
#11068=SHAPE_REPRESENTATION('',(#6038),#10931);
#11094=PRODUCT_DEFINITION_CONTEXT('part definition',#11186,'design');
#11099=PRODUCT_DEFINITION('Foot strip (1)','Foot strip (1)',#11129,#11094);
#11129=PRODUCT_DEFINITION_FORMATION('',$,#11192);
#11186=APPLICATION_CONTEXT(
'Core Data for Automotive Mechanical Design Process');
#11187=PRODUCT_CONTEXT('part definition',#11186,'mechanical');
#11192=PRODUCT('Foot strip (1)','Foot strip (1)','Foot strip (1)',(#11187));
#11267=COLOUR_RGB('Light Blue',0.38,0.62,0.78);
#11268=FILL_AREA_STYLE_COLOUR('',#11267);
#11269=FILL_AREA_STYLE('',(#11268));
#11270=SURFACE_STYLE_FILL_AREA(#11269);
#11271=SURFACE_SIDE_STYLE('',(#11270));
#11272=SURFACE_STYLE_USAGE(.BOTH.,#11271);
#11273=PRESENTATION_STYLE_ASSIGNMENT((#11272));
ENDSEC;
END-ISO-10303-21;
